ISO-10303-21;
HEADER;
FILE_DESCRIPTION (('STEP AP214'),
    '1' );
FILE_NAME ('Part 32,1_Varsayılan.step',
    '2026-10-10T17:45:43',
    ( '' ),
    ( '' ),
    'SwSTEP 2.0',
    'SolidWorks 2024',
    '' );
FILE_SCHEMA (( 'AUTOMOTIVE_DESIGN' ));
ENDSEC;

DATA;
#23=EDGE_CURVE ( 'NONE', #4236, #5003, #2060, .T. ) ;
#37=CARTESIAN_POINT ( 'NONE',  ( 172.0000000000000000, 68.99999999999998579, 0.000000000000000000 ) ) ;
#40=EDGE_CURVE ( 'NONE', #2876, #1030, #4508, .T. ) ;
#47=EDGE_CURVE ( 'NONE', #5003, #1574, #1946, .T. ) ;
#57=ORIENTED_EDGE ( 'NONE', *, *, #61, .F. ) ;
#61=EDGE_CURVE ( 'NONE', #5090, #3913, #5607, .T. ) ;
#85=CARTESIAN_POINT ( 'NONE',  ( 0.000000000000000000, 14.00000000000000000, 0.000000000000000000 ) ) ;
#100=EDGE_CURVE ( 'NONE', #5003, #2855, #4024, .T. ) ;
#109=CARTESIAN_POINT ( 'NONE',  ( 279.0000000000000000, 0.000000000000000000, 110.0000000000000000 ) ) ;
#111=AXIS2_PLACEMENT_3D ( 'NONE', #2275, #6279, #3332 ) ;
#117=VERTEX_POINT ( 'NONE', #4668 ) ;
#118=EDGE_CURVE ( 'NONE', #2855, #4195, #121, .T. ) ;
#119=EDGE_LOOP ( 'NONE', ( #1237, #139, #1625, #1192 ) ) ;
#121=CIRCLE ( 'NONE', #637, 24.99999999999999289 ) ;
#130=EDGE_CURVE ( 'NONE', #2876, #3788, #5065, .T. ) ;
#139=ORIENTED_EDGE ( 'NONE', *, *, #2354, .F. ) ;
#145=DIRECTION ( 'NONE',  ( 0.000000000000000000, -1.000000000000000000, 0.000000000000000000 ) ) ;
#154=DIRECTION ( 'NONE',  ( -1.000000000000000000, 0.000000000000000000, 0.000000000000000000 ) ) ;
#164=DIRECTION ( 'NONE',  ( -0.000000000000000000, -0.000000000000000000, 1.000000000000000000 ) ) ;
#167=APPLICATION_CONTEXT ( 'automotive_design' ) ;
#172=CARTESIAN_POINT ( 'NONE',  ( 67.00000000000000000, 69.00000000000000000, 110.0000000000000000 ) ) ;
#191=EDGE_CURVE ( 'NONE', #3657, #5057, #2480, .T. ) ;
#194=ORIENTED_EDGE ( 'NONE', *, *, #3413, .T. ) ;
#198=CARTESIAN_POINT ( 'NONE',  ( 0.000000000000000000, 14.00000000000000000, 110.0000000000000000 ) ) ;
#208=ADVANCED_FACE ( 'NONE', ( #366 ), #2251, .F. ) ;
#228=SHAPE_REPRESENTATION_RELATIONSHIP ( 'NONE' , 'NONE' ,  #2313, #2933 ) ;
#290=CARTESIAN_POINT ( 'NONE',  ( 0.000000000000000000, 0.000000000000000000, 0.000000000000000000 ) ) ;
#322=EDGE_CURVE ( 'NONE', #5682, #117, #4160, .T. ) ;
#331=DIRECTION ( 'NONE',  ( -0.000000000000000000, -0.000000000000000000, -1.000000000000000000 ) ) ;
#333=DIRECTION ( 'NONE',  ( -1.000000000000000000, 0.000000000000000000, 0.000000000000000000 ) ) ;
#339=CARTESIAN_POINT ( 'NONE',  ( 132.0000000000000000, 69.00000000000000000, 0.000000000000000000 ) ) ;
#345=CARTESIAN_POINT ( 'NONE',  ( 265.0000000000000000, 0.000000000000000000, 110.0000000000000000 ) ) ;
#360=DIRECTION ( 'NONE',  ( -0.000000000000000000, -0.000000000000000000, -1.000000000000000000 ) ) ;
#362=ORIENTED_EDGE ( 'NONE', *, *, #5906, .F. ) ;
#366=FACE_OUTER_BOUND ( 'NONE', #4514, .T. ) ;
#375=AXIS2_PLACEMENT_3D ( 'NONE', #3837, #2921, #5808 ) ;
#384=CARTESIAN_POINT ( 'NONE',  ( 14.00000000000000000, 14.00000000000000000, 110.0000000000000000 ) ) ;
#389=( GEOMETRIC_REPRESENTATION_CONTEXT ( 3 ) GLOBAL_UNCERTAINTY_ASSIGNED_CONTEXT ( ( #5158 ) ) GLOBAL_UNIT_ASSIGNED_CONTEXT ( ( #5187, #2278, #1180 ) ) REPRESENTATION_CONTEXT ( 'NONE', 'WORKASPACE' ) );
#400=AXIS2_PLACEMENT_3D ( 'NONE', #2031, #1061, #2896 ) ;
#407=ORIENTED_EDGE ( 'NONE', *, *, #5272, .F. ) ;
#409=CARTESIAN_POINT ( 'NONE',  ( 42.00000000000000000, 69.00000000000000000, 110.0000000000000000 ) ) ;
#412=LINE ( 'NONE', #3355, #3285 ) ;
#432=ORIENTED_EDGE ( 'NONE', *, *, #4266, .F. ) ;
#452=CARTESIAN_POINT ( 'NONE',  ( 14.00000000000000000, 0.000000000000000000, 0.000000000000000000 ) ) ;
#455=PLANE ( 'NONE',  #375 ) ;
#465=FACE_OUTER_BOUND ( 'NONE', #4295, .T. ) ;
#472=ADVANCED_FACE ( 'NONE', ( #5860 ), #5405, .F. ) ;
#475=LINE ( 'NONE', #892, #5466 ) ;
#497=CARTESIAN_POINT ( 'NONE',  ( 262.0000000000000000, 68.99999999999997158, 110.0000000000000000 ) ) ;
#499=EDGE_CURVE ( 'NONE', #2855, #4961, #475, .T. ) ;
#522=CARTESIAN_POINT ( 'NONE',  ( 265.0000000000000000, 0.000000000000000000, 0.000000000000000000 ) ) ;
#534=EDGE_LOOP ( 'NONE', ( #3667, #4259, #1985, #3531 ) ) ;
#584=FACE_OUTER_BOUND ( 'NONE', #5731, .T. ) ;
#590=VERTEX_POINT ( 'NONE', #5560 ) ;
#630=VECTOR ( 'NONE', #6353, 1000.000000000000000 ) ;
#634=ORIENTED_EDGE ( 'NONE', *, *, #6210, .T. ) ;
#637=AXIS2_PLACEMENT_3D ( 'NONE', #2186, #6003, #1185 ) ;
#654=VECTOR ( 'NONE', #851, 1000.000000000000000 ) ;
#659=ORIENTED_EDGE ( 'NONE', *, *, #4580, .F. ) ;
#668=DIRECTION ( 'NONE',  ( 0.000000000000000000, -0.000000000000000000, -1.000000000000000000 ) ) ;
#682=AXIS2_PLACEMENT_3D ( 'NONE', #37, #2481, #5417 ) ;
#696=ORIENTED_EDGE ( 'NONE', *, *, #2847, .F. ) ;
#726=CARTESIAN_POINT ( 'NONE',  ( 82.00000000000001421, 69.00000000000000000, 110.0000000000000000 ) ) ;
#742=ORIENTED_EDGE ( 'NONE', *, *, #1261, .T. ) ;
#749=CARTESIAN_POINT ( 'NONE',  ( 14.00000000000000000, 14.00000000000000000, 110.0000000000000000 ) ) ;
#756=DIRECTION ( 'NONE',  ( -1.000000000000000000, -0.000000000000000000, -0.000000000000000000 ) ) ;
#767=CARTESIAN_POINT ( 'NONE',  ( 197.0000000000000000, 68.99999999999997158, 110.0000000000000000 ) ) ;
#776=EDGE_CURVE ( 'NONE', #3357, #6130, #2680, .T. ) ;
#782=ORIENTED_EDGE ( 'NONE', *, *, #4549, .T. ) ;
#784=DIRECTION ( 'NONE',  ( -0.000000000000000000, -0.000000000000000000, -1.000000000000000000 ) ) ;
#838=CLOSED_SHELL ( 'NONE', ( #3926, #472, #2141, #4596, #6202, #3144, #3539, #5587, #5826, #2784, #995, #5539, #2322, #208, #1807, #4835 ) ) ;
#844=CARTESIAN_POINT ( 'NONE',  ( 237.0000000000000284, 68.99999999999997158, 110.0000000000000000 ) ) ;
#851=DIRECTION ( 'NONE',  ( -0.000000000000000000, -0.000000000000000000, -1.000000000000000000 ) ) ;
#860=EDGE_CURVE ( 'NONE', #590, #5090, #4386, .T. ) ;
#864=VECTOR ( 'NONE', #784, 1000.000000000000000 ) ;
#874=DIRECTION ( 'NONE',  ( 1.000000000000000000, 0.000000000000000000, 0.000000000000000000 ) ) ;
#880=DIRECTION ( 'NONE',  ( 0.000000000000000000, 0.000000000000000000, 1.000000000000000000 ) ) ;
#892=CARTESIAN_POINT ( 'NONE',  ( 132.0000000000000000, 69.00000000000000000, 110.0000000000000000 ) ) ;
#894=VECTOR ( 'NONE', #3755, 1000.000000000000000 ) ;
#895=FACE_OUTER_BOUND ( 'NONE', #119, .T. ) ;
#898=ORIENTED_EDGE ( 'NONE', *, *, #776, .F. ) ;
#919=VECTOR ( 'NONE', #5261, 1000.000000000000000 ) ;
#935=CARTESIAN_POINT ( 'NONE',  ( 67.00000000000000000, 69.00000000000000000, 110.0000000000000000 ) ) ;
#952=DIRECTION ( 'NONE',  ( 1.000000000000000000, 0.000000000000000000, 0.000000000000000000 ) ) ;
#976=ORIENTED_EDGE ( 'NONE', *, *, #1918, .F. ) ;
#991=CARTESIAN_POINT ( 'NONE',  ( 0.000000000000000000, 0.000000000000000000, 110.0000000000000000 ) ) ;
#995=ADVANCED_FACE ( 'NONE', ( #465 ), #2424, .F. ) ;
#1030=VERTEX_POINT ( 'NONE', #6356 ) ;
#1061=DIRECTION ( 'NONE',  ( -0.000000000000000000, -0.000000000000000000, -1.000000000000000000 ) ) ;
#1078=AXIS2_PLACEMENT_3D ( 'NONE', #6011, #4579, #3617 ) ;
#1101=VECTOR ( 'NONE', #3349, 1000.000000000000000 ) ;
#1122=EDGE_CURVE ( 'NONE', #117, #5057, #4136, .T. ) ;
#1125=VECTOR ( 'NONE', #5931, 1000.000000000000000 ) ;
#1128=DIRECTION ( 'NONE',  ( 0.000000000000000000, -0.000000000000000000, -1.000000000000000000 ) ) ;
#1144=VERTEX_POINT ( 'NONE', #6088 ) ;
#1151=CARTESIAN_POINT ( 'NONE',  ( 14.00000000000000000, 0.000000000000000000, 110.0000000000000000 ) ) ;
#1163=VERTEX_POINT ( 'NONE', #1666 ) ;
#1170=CARTESIAN_POINT ( 'NONE',  ( 17.00000000000000000, 69.00000000000000000, 110.0000000000000000 ) ) ;
#1180=( NAMED_UNIT ( * ) SI_UNIT ( $, .STERADIAN. ) SOLID_ANGLE_UNIT ( ) );
#1185=DIRECTION ( 'NONE',  ( 1.000000000000000000, 0.000000000000000000, 0.000000000000000000 ) ) ;
#1192=ORIENTED_EDGE ( 'NONE', *, *, #2097, .F. ) ;
#1198=CARTESIAN_POINT ( 'NONE',  ( 212.0000000000000284, 68.99999999999997158, 110.0000000000000000 ) ) ;
#1237=ORIENTED_EDGE ( 'NONE', *, *, #6018, .F. ) ;
#1261=EDGE_CURVE ( 'NONE', #3657, #2635, #3181, .T. ) ;
#1267=FACE_OUTER_BOUND ( 'NONE', #2381, .T. ) ;
#1279=DIRECTION ( 'NONE',  ( -1.000000000000000000, 0.000000000000000000, 0.000000000000000000 ) ) ;
#1282=CYLINDRICAL_SURFACE ( 'NONE', #2740, 24.99999999999999289 ) ;
#1285=DIRECTION ( 'NONE',  ( 0.000000000000000000, -1.000000000000000000, 0.000000000000000000 ) ) ;
#1299=DIRECTION ( 'NONE',  ( -0.000000000000000000, -1.000000000000000000, -0.000000000000000000 ) ) ;
#1319=DIRECTION ( 'NONE',  ( 1.000000000000000000, 0.000000000000000000, 0.000000000000000000 ) ) ;
#1320=CARTESIAN_POINT ( 'NONE',  ( 279.0000000000000000, 68.99999999999997158, 0.000000000000000000 ) ) ;
#1323=EDGE_CURVE ( 'NONE', #1030, #2050, #2693, .T. ) ;
#1353=LINE ( 'NONE', #3282, #3912 ) ;
#1359=LINE ( 'NONE', #726, #864 ) ;
#1365=DIRECTION ( 'NONE',  ( -1.000000000000000000, 0.000000000000000000, 0.000000000000000000 ) ) ;
#1417=FACE_OUTER_BOUND ( 'NONE', #2458, .T. ) ;
#1422=CARTESIAN_POINT ( 'NONE',  ( 0.000000000000000000, 69.00000000000000000, 110.0000000000000000 ) ) ;
#1454=AXIS2_PLACEMENT_3D ( 'NONE', #6194, #880, #2217 ) ;
#1464=DIRECTION ( 'NONE',  ( 0.000000000000000000, 0.000000000000000000, -1.000000000000000000 ) ) ;
#1468=FACE_OUTER_BOUND ( 'NONE', #4320, .T. ) ;
#1474=CARTESIAN_POINT ( 'NONE',  ( 147.0000000000000284, 69.00000000000000000, 110.0000000000000000 ) ) ;
#1485=CYLINDRICAL_SURFACE ( 'NONE', #400, 24.99999999999999289 ) ;
#1497=ORIENTED_EDGE ( 'NONE', *, *, #118, .T. ) ;
#1540=AXIS2_PLACEMENT_3D ( 'NONE', #1749, #145, #2190 ) ;
#1543=ORIENTED_EDGE ( 'NONE', *, *, #3879, .T. ) ;
#1574=VERTEX_POINT ( 'NONE', #1595 ) ;
#1576=CARTESIAN_POINT ( 'NONE',  ( 279.0000000000000000, 14.00000000000000000, 110.0000000000000000 ) ) ;
#1586=DIRECTION ( 'NONE',  ( 1.000000000000000000, 0.000000000000000000, 0.000000000000000000 ) ) ;
#1591=EDGE_CURVE ( 'NONE', #1163, #3913, #3969, .T. ) ;
#1595=CARTESIAN_POINT ( 'NONE',  ( 147.0000000000000284, 69.00000000000000000, 0.000000000000000000 ) ) ;
#1613=VECTOR ( 'NONE', #3858, 1000.000000000000000 ) ;
#1625=ORIENTED_EDGE ( 'NONE', *, *, #191, .F. ) ;
#1627=MECHANICAL_DESIGN_GEOMETRIC_PRESENTATION_REPRESENTATION('',(#6060),#5240);
#1636=PLANE ( 'NONE',  #4478 ) ;
#1647=EDGE_CURVE ( 'NONE', #4666, #2876, #3243, .T. ) ;
#1650=PLANE ( 'NONE',  #1540 ) ;
#1665=ORIENTED_EDGE ( 'NONE', *, *, #3879, .F. ) ;
#1666=CARTESIAN_POINT ( 'NONE',  ( 262.0000000000000000, 68.99999999999997158, 0.000000000000000000 ) ) ;
#1673=CARTESIAN_POINT ( 'NONE',  ( 212.0000000000000284, 68.99999999999997158, 110.0000000000000000 ) ) ;
#1681=PRODUCT ( 'Part 32,1_Varsay\X2\0131\X0\lan', 'Part 32,1_Varsay\X2\0131\X0\lan', '', ( #5150 ) ) ;
#1684=DIRECTION ( 'NONE',  ( 0.000000000000000000, -1.000000000000000000, 0.000000000000000000 ) ) ;
#1699=DIRECTION ( 'NONE',  ( 1.000000000000000000, 0.000000000000000000, 0.000000000000000000 ) ) ;
#1706=ORIENTED_EDGE ( 'NONE', *, *, #1918, .T. ) ;
#1733=UNCERTAINTY_MEASURE_WITH_UNIT (LENGTH_MEASURE( 1.000000000000000082E-05 ), #3154, 'distance_accuracy_value', 'NONE');
#1736=CARTESIAN_POINT ( 'NONE',  ( 67.00000000000000000, 69.00000000000000000, 0.000000000000000000 ) ) ;
#1744=PRODUCT_DEFINITION_SHAPE ( 'NONE', 'NONE',  #2790 ) ;
#1749=CARTESIAN_POINT ( 'NONE',  ( 197.0000000000000000, 68.99999999999997158, 110.0000000000000000 ) ) ;
#1776=CARTESIAN_POINT ( 'NONE',  ( 14.00000000000000000, 0.000000000000000000, 110.0000000000000000 ) ) ;
#1780=ORIENTED_EDGE ( 'NONE', *, *, #776, .T. ) ;
#1783=DIRECTION ( 'NONE',  ( 1.000000000000000000, 0.000000000000000000, 0.000000000000000000 ) ) ;
#1788=ORIENTED_EDGE ( 'NONE', *, *, #100, .F. ) ;
#1795=EDGE_LOOP ( 'NONE', ( #3572, #4949, #362, #4274 ) ) ;
#1807=ADVANCED_FACE ( 'NONE', ( #1267 ), #3227, .T. ) ;
#1808=CARTESIAN_POINT ( 'NONE',  ( 67.00000000000000000, 69.00000000000000000, 110.0000000000000000 ) ) ;
#1822=LINE ( 'NONE', #345, #5035 ) ;
#1841=CARTESIAN_POINT ( 'NONE',  ( 265.0000000000000000, 0.000000000000000000, 110.0000000000000000 ) ) ;
#1851=ORIENTED_EDGE ( 'NONE', *, *, #3532, .F. ) ;
#1865=AXIS2_PLACEMENT_3D ( 'NONE', #991, #3824, #3397 ) ;
#1867=ORIENTED_EDGE ( 'NONE', *, *, #4266, .T. ) ;
#1901=ORIENTED_EDGE ( 'NONE', *, *, #6210, .F. ) ;
#1918=EDGE_CURVE ( 'NONE', #4195, #3357, #1359, .T. ) ;
#1931=CARTESIAN_POINT ( 'NONE',  ( 0.000000000000000000, 0.000000000000000000, 110.0000000000000000 ) ) ;
#1937=EDGE_CURVE ( 'NONE', #5271, #117, #4669, .T. ) ;
#1946=LINE ( 'NONE', #3387, #630 ) ;
#1960=ORIENTED_EDGE ( 'NONE', *, *, #322, .F. ) ;
#1967=ORIENTED_EDGE ( 'NONE', *, *, #2075, .T. ) ;
#1985=ORIENTED_EDGE ( 'NONE', *, *, #23, .F. ) ;
#2002=LINE ( 'NONE', #497, #2363 ) ;
#2031=CARTESIAN_POINT ( 'NONE',  ( 107.0000000000000142, 69.00000000000000000, 110.0000000000000000 ) ) ;
#2050=VERTEX_POINT ( 'NONE', #1320 ) ;
#2058=VECTOR ( 'NONE', #2660, 1000.000000000000000 ) ;
#2060=CIRCLE ( 'NONE', #2160, 24.99999999999999289 ) ;
#2067=DIRECTION ( 'NONE',  ( 0.000000000000000000, 1.000000000000000000, 0.000000000000000000 ) ) ;
#2074=VECTOR ( 'NONE', #874, 1000.000000000000000 ) ;
#2075=EDGE_CURVE ( 'NONE', #4556, #4140, #4342, .T. ) ;
#2097=EDGE_CURVE ( 'NONE', #3522, #3657, #2320, .T. ) ;
#2099=ORIENTED_EDGE ( 'NONE', *, *, #2473, .T. ) ;
#2140=CIRCLE ( 'NONE', #4302, 14.00000000000001243 ) ;
#2141=ADVANCED_FACE ( 'NONE', ( #4865 ), #455, .F. ) ;
#2160=AXIS2_PLACEMENT_3D ( 'NONE', #3450, #2490, #952 ) ;
#2163=EDGE_LOOP ( 'NONE', ( #1780, #1901, #2945, #1706 ) ) ;
#2184=DIRECTION ( 'NONE',  ( 1.000000000000000000, 0.000000000000000000, 0.000000000000000000 ) ) ;
#2186=CARTESIAN_POINT ( 'NONE',  ( 107.0000000000000142, 69.00000000000000000, 110.0000000000000000 ) ) ;
#2189=DIRECTION ( 'NONE',  ( 0.000000000000000000, -1.000000000000000000, 0.000000000000000000 ) ) ;
#2190=DIRECTION ( 'NONE',  ( 0.000000000000000000, -0.000000000000000000, -1.000000000000000000 ) ) ;
#2217=DIRECTION ( 'NONE',  ( 1.000000000000000000, 0.000000000000000000, -0.000000000000000000 ) ) ;
#2242=DIRECTION ( 'NONE',  ( 0.000000000000000000, 0.000000000000000000, 1.000000000000000000 ) ) ;
#2251=PLANE ( 'NONE',  #1454 ) ;
#2256=ORIENTED_EDGE ( 'NONE', *, *, #2544, .T. ) ;
#2265=EDGE_CURVE ( 'NONE', #5889, #1574, #5612, .T. ) ;
#2275=CARTESIAN_POINT ( 'NONE',  ( 0.000000000000000000, 0.000000000000000000, 110.0000000000000000 ) ) ;
#2278=( NAMED_UNIT ( * ) PLANE_ANGLE_UNIT ( ) SI_UNIT ( $, .RADIAN. ) );
#2287=DIRECTION ( 'NONE',  ( 1.000000000000000000, 0.000000000000000000, 0.000000000000000000 ) ) ;
#2305=DIRECTION ( 'NONE',  ( 0.000000000000000000, 0.000000000000000000, -1.000000000000000000 ) ) ;
#2313=SHAPE_REPRESENTATION ( 'Part 32,1_Varsay\X2\0131\X0\lan', ( #6349 ), #389 ) ;
#2314=DIRECTION ( 'NONE',  ( -1.000000000000000000, 0.000000000000000000, 0.000000000000000000 ) ) ;
#2319=DIRECTION ( 'NONE',  ( -0.000000000000000000, -0.000000000000000000, -1.000000000000000000 ) ) ;
#2320=LINE ( 'NONE', #1776, #3111 ) ;
#2322=ADVANCED_FACE ( 'NONE', ( #584 ), #1636, .T. ) ;
#2328=AXIS2_PLACEMENT_3D ( 'NONE', #409, #4325, #1365 ) ;
#2334=ORIENTED_EDGE ( 'NONE', *, *, #1647, .T. ) ;
#2339=VECTOR ( 'NONE', #5809, 1000.000000000000000 ) ;
#2354=EDGE_CURVE ( 'NONE', #5057, #1144, #4018, .T. ) ;
#2355=LINE ( 'NONE', #4316, #2339 ) ;
#2360=CARTESIAN_POINT ( 'NONE',  ( 197.0000000000000000, 68.99999999999997158, 110.0000000000000000 ) ) ;
#2362=CARTESIAN_POINT ( 'NONE',  ( 265.0000000000000000, 14.00000000000000000, 110.0000000000000000 ) ) ;
#2363=VECTOR ( 'NONE', #3514, 1000.000000000000000 ) ;
#2375=ORIENTED_EDGE ( 'NONE', *, *, #191, .T. ) ;
#2381=EDGE_LOOP ( 'NONE', ( #2736, #407, #4709, #3732 ) ) ;
#2412=LINE ( 'NONE', #2477, #1125 ) ;
#2416=DIRECTION ( 'NONE',  ( -1.000000000000000000, -0.000000000000000000, -0.000000000000000000 ) ) ;
#2424=CYLINDRICAL_SURFACE ( 'NONE', #2328, 25.00000000000000000 ) ;
#2431=DIRECTION ( 'NONE',  ( -0.000000000000000000, -0.000000000000000000, -1.000000000000000000 ) ) ;
#2439=FACE_OUTER_BOUND ( 'NONE', #534, .T. ) ;
#2458=EDGE_LOOP ( 'NONE', ( #5298, #6141, #3579, #5465 ) ) ;
#2473=EDGE_CURVE ( 'NONE', #1030, #590, #3737, .T. ) ;
#2477=CARTESIAN_POINT ( 'NONE',  ( 197.0000000000000000, 68.99999999999997158, 0.000000000000000000 ) ) ;
#2480=CIRCLE ( 'NONE', #2883, 14.00000000000000000 ) ;
#2481=DIRECTION ( 'NONE',  ( -0.000000000000000000, -0.000000000000000000, -1.000000000000000000 ) ) ;
#2490=DIRECTION ( 'NONE',  ( -0.000000000000000000, -0.000000000000000000, -1.000000000000000000 ) ) ;
#2514=CARTESIAN_POINT ( 'NONE',  ( 82.00000000000001421, 69.00000000000000000, 0.000000000000000000 ) ) ;
#2544=EDGE_CURVE ( 'NONE', #4961, #3357, #5323, .T. ) ;
#2620=ORIENTED_EDGE ( 'NONE', *, *, #6018, .T. ) ;
#2630=VECTOR ( 'NONE', #1279, 1000.000000000000000 ) ;
#2635=VERTEX_POINT ( 'NONE', #522 ) ;
#2658=AXIS2_PLACEMENT_3D ( 'NONE', #384, #2305, #5284 ) ;
#2660=DIRECTION ( 'NONE',  ( 0.000000000000000000, 1.000000000000000000, 0.000000000000000000 ) ) ;
#2680=LINE ( 'NONE', #5175, #894 ) ;
#2693=LINE ( 'NONE', #2796, #4333 ) ;
#2700=DIRECTION ( 'NONE',  ( -0.000000000000000000, -0.000000000000000000, -1.000000000000000000 ) ) ;
#2732=CIRCLE ( 'NONE', #3162, 14.00000000000000000 ) ;
#2736=ORIENTED_EDGE ( 'NONE', *, *, #1647, .F. ) ;
#2740=AXIS2_PLACEMENT_3D ( 'NONE', #844, #360, #2314 ) ;
#2745=ORIENTED_EDGE ( 'NONE', *, *, #5272, .T. ) ;
#2767=DIRECTION ( 'NONE',  ( -1.000000000000000000, -0.000000000000000000, -0.000000000000000000 ) ) ;
#2775=CARTESIAN_POINT ( 'NONE',  ( 0.000000000000000000, 69.00000000000000000, 110.0000000000000000 ) ) ;
#2784=ADVANCED_FACE ( 'NONE', ( #6107 ), #5109, .F. ) ;
#2790=PRODUCT_DEFINITION ( 'UNKNOWN', '', #6116, #5010 ) ;
#2796=CARTESIAN_POINT ( 'NONE',  ( 279.0000000000000000, 68.99999999999997158, 110.0000000000000000 ) ) ;
#2808=ORIENTED_EDGE ( 'NONE', *, *, #2847, .T. ) ;
#2814=ORIENTED_EDGE ( 'NONE', *, *, #1591, .F. ) ;
#2832=EDGE_LOOP ( 'NONE', ( #2256, #976, #5186, #3086 ) ) ;
#2847=EDGE_CURVE ( 'NONE', #5271, #1144, #412, .T. ) ;
#2855=VERTEX_POINT ( 'NONE', #4357 ) ;
#2875=CARTESIAN_POINT ( 'NONE',  ( 279.0000000000000000, 14.00000000000000000, 110.0000000000000000 ) ) ;
#2876=VERTEX_POINT ( 'NONE', #2875 ) ;
#2883=AXIS2_PLACEMENT_3D ( 'NONE', #4220, #2319, #1319 ) ;
#2893=( NAMED_UNIT ( * ) SI_UNIT ( $, .STERADIAN. ) SOLID_ANGLE_UNIT ( ) );
#2896=DIRECTION ( 'NONE',  ( -1.000000000000000000, 0.000000000000000000, 0.000000000000000000 ) ) ;
#2921=DIRECTION ( 'NONE',  ( -1.000000000000000000, 0.000000000000000000, 0.000000000000000000 ) ) ;
#2933=ADVANCED_BREP_SHAPE_REPRESENTATION ( '', ( #4588, #6349 ), #389 ) ;
#2937=PLANE ( 'NONE',  #3787 ) ;
#2945=ORIENTED_EDGE ( 'NONE', *, *, #4656, .F. ) ;
#2961=VECTOR ( 'NONE', #2767, 1000.000000000000000 ) ;
#2980=ORIENTED_EDGE ( 'NONE', *, *, #860, .T. ) ;
#3006=DIRECTION ( 'NONE',  ( -1.000000000000000000, 0.000000000000000000, 0.000000000000000000 ) ) ;
#3085=CARTESIAN_POINT ( 'NONE',  ( 237.0000000000000284, 68.99999999999997158, 0.000000000000000000 ) ) ;
#3086=ORIENTED_EDGE ( 'NONE', *, *, #499, .T. ) ;
#3090=CARTESIAN_POINT ( 'NONE',  ( 42.00000000000000000, 69.00000000000000000, 110.0000000000000000 ) ) ;
#3111=VECTOR ( 'NONE', #3222, 1000.000000000000000 ) ;
#3141=ORIENTED_EDGE ( 'NONE', *, *, #6249, .T. ) ;
#3144=ADVANCED_FACE ( 'NONE', ( #4673 ), #1650, .F. ) ;
#3149=DIRECTION ( 'NONE',  ( -0.000000000000000000, -1.000000000000000000, -0.000000000000000000 ) ) ;
#3153=VECTOR ( 'NONE', #6340, 1000.000000000000000 ) ;
#3154=( LENGTH_UNIT ( ) NAMED_UNIT ( * ) SI_UNIT ( .MILLI., .METRE. ) );
#3162=AXIS2_PLACEMENT_3D ( 'NONE', #749, #4111, #4503 ) ;
#3181=LINE ( 'NONE', #3770, #2074 ) ;
#3222=DIRECTION ( 'NONE',  ( 0.000000000000000000, 0.000000000000000000, -1.000000000000000000 ) ) ;
#3227=CYLINDRICAL_SURFACE ( 'NONE', #4548, 14.00000000000001243 ) ;
#3232=ORIENTED_EDGE ( 'NONE', *, *, #2075, .F. ) ;
#3243=CIRCLE ( 'NONE', #1078, 14.00000000000001243 ) ;
#3282=CARTESIAN_POINT ( 'NONE',  ( 279.0000000000000000, 68.99999999999997158, 0.000000000000000000 ) ) ;
#3285=VECTOR ( 'NONE', #1299, 1000.000000000000000 ) ;
#3313=( NAMED_UNIT ( * ) PLANE_ANGLE_UNIT ( ) SI_UNIT ( $, .RADIAN. ) );
#3332=DIRECTION ( 'NONE',  ( 0.000000000000000000, 0.000000000000000000, -1.000000000000000000 ) ) ;
#3349=DIRECTION ( 'NONE',  ( -1.000000000000000000, -0.000000000000000000, -0.000000000000000000 ) ) ;
#3355=CARTESIAN_POINT ( 'NONE',  ( 0.000000000000000000, 0.000000000000000000, 110.0000000000000000 ) ) ;
#3357=VERTEX_POINT ( 'NONE', #2514 ) ;
#3387=CARTESIAN_POINT ( 'NONE',  ( 147.0000000000000284, 69.00000000000000000, 110.0000000000000000 ) ) ;
#3397=DIRECTION ( 'NONE',  ( 0.000000000000000000, -0.000000000000000000, 1.000000000000000000 ) ) ;
#3413=EDGE_CURVE ( 'NONE', #590, #1163, #2002, .T. ) ;
#3416=FACE_OUTER_BOUND ( 'NONE', #2832, .T. ) ;
#3424=ORIENTED_EDGE ( 'NONE', *, *, #5906, .T. ) ;
#3434=CARTESIAN_POINT ( 'NONE',  ( 132.0000000000000000, 69.00000000000000000, 0.000000000000000000 ) ) ;
#3450=CARTESIAN_POINT ( 'NONE',  ( 172.0000000000000000, 68.99999999999998579, 110.0000000000000000 ) ) ;
#3476=ORIENTED_EDGE ( 'NONE', *, *, #130, .T. ) ;
#3491=DIRECTION ( 'NONE',  ( 0.000000000000000000, -0.000000000000000000, -1.000000000000000000 ) ) ;
#3514=DIRECTION ( 'NONE',  ( -0.000000000000000000, -0.000000000000000000, -1.000000000000000000 ) ) ;
#3519=FACE_OUTER_BOUND ( 'NONE', #1795, .T. ) ;
#3522=VERTEX_POINT ( 'NONE', #1151 ) ;
#3531=ORIENTED_EDGE ( 'NONE', *, *, #5749, .T. ) ;
#3532=EDGE_CURVE ( 'NONE', #2050, #1163, #1353, .T. ) ;
#3539=ADVANCED_FACE ( 'NONE', ( #2439 ), #4552, .F. ) ;
#3558=LINE ( 'NONE', #5899, #1613 ) ;
#3572=ORIENTED_EDGE ( 'NONE', *, *, #322, .T. ) ;
#3574=CARTESIAN_POINT ( 'NONE',  ( 132.0000000000000000, 69.00000000000000000, 110.0000000000000000 ) ) ;
#3579=ORIENTED_EDGE ( 'NONE', *, *, #2473, .F. ) ;
#3594=DIRECTION ( 'NONE',  ( 1.000000000000000000, 0.000000000000000000, 0.000000000000000000 ) ) ;
#3596=LINE ( 'NONE', #4561, #2058 ) ;
#3606=VECTOR ( 'NONE', #756, 1000.000000000000000 ) ;
#3617=DIRECTION ( 'NONE',  ( 1.000000000000000000, 0.000000000000000000, 0.000000000000000000 ) ) ;
#3624=CARTESIAN_POINT ( 'NONE',  ( 0.000000000000000000, 69.00000000000000000, 0.000000000000000000 ) ) ;
#3629=EDGE_CURVE ( 'NONE', #3913, #5889, #2412, .T. ) ;
#3657=VERTEX_POINT ( 'NONE', #452 ) ;
#3667=ORIENTED_EDGE ( 'NONE', *, *, #2265, .T. ) ;
#3699=APPLICATION_CONTEXT ( 'automotive_design' ) ;
#3714=VECTOR ( 'NONE', #5511, 1000.000000000000000 ) ;
#3717=ORIENTED_EDGE ( 'NONE', *, *, #5698, .F. ) ;
#3732=ORIENTED_EDGE ( 'NONE', *, *, #130, .F. ) ;
#3737=LINE ( 'NONE', #5699, #2630 ) ;
#3755=DIRECTION ( 'NONE',  ( -1.000000000000000000, -0.000000000000000000, -0.000000000000000000 ) ) ;
#3770=CARTESIAN_POINT ( 'NONE',  ( 0.000000000000000000, 0.000000000000000000, 0.000000000000000000 ) ) ;
#3771=FACE_OUTER_BOUND ( 'NONE', #5518, .T. ) ;
#3787=AXIS2_PLACEMENT_3D ( 'NONE', #4427, #2189, #1128 ) ;
#3788=VERTEX_POINT ( 'NONE', #5056 ) ;
#3824=DIRECTION ( 'NONE',  ( 0.000000000000000000, 1.000000000000000000, 0.000000000000000000 ) ) ;
#3826=VECTOR ( 'NONE', #3149, 1000.000000000000000 ) ;
#3837=CARTESIAN_POINT ( 'NONE',  ( 279.0000000000000000, 0.000000000000000000, 110.0000000000000000 ) ) ;
#3849=ORIENTED_EDGE ( 'NONE', *, *, #2265, .F. ) ;
#3858=DIRECTION ( 'NONE',  ( -0.000000000000000000, -0.000000000000000000, -1.000000000000000000 ) ) ;
#3879=EDGE_CURVE ( 'NONE', #3788, #2050, #3596, .T. ) ;
#3912=VECTOR ( 'NONE', #333, 1000.000000000000000 ) ;
#3913=VERTEX_POINT ( 'NONE', #4070 ) ;
#3917=VECTOR ( 'NONE', #2067, 1000.000000000000000 ) ;
#3926=ADVANCED_FACE ( 'NONE', ( #4728 ), #5285, .F. ) ;
#3929=DIRECTION ( 'NONE',  ( -0.000000000000000000, -0.000000000000000000, -1.000000000000000000 ) ) ;
#3946=CARTESIAN_POINT ( 'NONE',  ( 0.000000000000000000, 69.00000000000000000, 110.0000000000000000 ) ) ;
#3963=CARTESIAN_POINT ( 'NONE',  ( 197.0000000000000000, 68.99999999999997158, 0.000000000000000000 ) ) ;
#3969=CIRCLE ( 'NONE', #4577, 24.99999999999999289 ) ;
#3981=AXIS2_PLACEMENT_3D ( 'NONE', #3946, #5949, #3491 ) ;
#4016=ORIENTED_EDGE ( 'NONE', *, *, #40, .F. ) ;
#4018=LINE ( 'NONE', #198, #4051 ) ;
#4023=ORIENTED_EDGE ( 'NONE', *, *, #1937, .T. ) ;
#4024=LINE ( 'NONE', #3574, #3606 ) ;
#4034=LINE ( 'NONE', #1931, #5115 ) ;
#4051=VECTOR ( 'NONE', #164, 1000.000000000000000 ) ;
#4060=CARTESIAN_POINT ( 'NONE',  ( 172.0000000000000000, 68.99999999999998579, 110.0000000000000000 ) ) ;
#4070=CARTESIAN_POINT ( 'NONE',  ( 212.0000000000000284, 68.99999999999997158, 0.000000000000000000 ) ) ;
#4095=AXIS2_PLACEMENT_3D ( 'NONE', #5079, #1684, #668 ) ;
#4111=DIRECTION ( 'NONE',  ( 0.000000000000000000, 0.000000000000000000, 1.000000000000000000 ) ) ;
#4115=DIRECTION ( 'NONE',  ( -0.000000000000000000, -0.000000000000000000, -1.000000000000000000 ) ) ;
#4121=ORIENTED_EDGE ( 'NONE', *, *, #5749, .F. ) ;
#4136=LINE ( 'NONE', #5575, #3826 ) ;
#4140=VERTEX_POINT ( 'NONE', #1170 ) ;
#4160=LINE ( 'NONE', #3624, #5139 ) ;
#4165=AXIS2_PLACEMENT_3D ( 'NONE', #6203, #4582, #1783 ) ;
#4167=VECTOR ( 'NONE', #2416, 1000.000000000000000 ) ;
#4169=DIRECTION ( 'NONE',  ( 1.000000000000000000, 0.000000000000000000, 0.000000000000000000 ) ) ;
#4195=VERTEX_POINT ( 'NONE', #5080 ) ;
#4220=CARTESIAN_POINT ( 'NONE',  ( 14.00000000000000000, 14.00000000000000000, 0.000000000000000000 ) ) ;
#4234=SHAPE_DEFINITION_REPRESENTATION ( #1744, #2313 ) ;
#4236=VERTEX_POINT ( 'NONE', #767 ) ;
#4249=LINE ( 'NONE', #339, #2961 ) ;
#4259=ORIENTED_EDGE ( 'NONE', *, *, #47, .F. ) ;
#4266=EDGE_CURVE ( 'NONE', #5090, #4236, #4870, .T. ) ;
#4274=ORIENTED_EDGE ( 'NONE', *, *, #6219, .T. ) ;
#4295=EDGE_LOOP ( 'NONE', ( #4468, #4611, #3232, #634 ) ) ;
#4299=CYLINDRICAL_SURFACE ( 'NONE', #2658, 14.00000000000000000 ) ;
#4302=AXIS2_PLACEMENT_3D ( 'NONE', #4638, #5063, #2184 ) ;
#4316=CARTESIAN_POINT ( 'NONE',  ( 197.0000000000000000, 68.99999999999997158, 110.0000000000000000 ) ) ;
#4320=EDGE_LOOP ( 'NONE', ( #4350, #5793, #1788, #5134 ) ) ;
#4325=DIRECTION ( 'NONE',  ( -0.000000000000000000, -0.000000000000000000, -1.000000000000000000 ) ) ;
#4333=VECTOR ( 'NONE', #331, 1000.000000000000000 ) ;
#4342=CIRCLE ( 'NONE', #6002, 25.00000000000000000 ) ;
#4350=ORIENTED_EDGE ( 'NONE', *, *, #5698, .T. ) ;
#4357=CARTESIAN_POINT ( 'NONE',  ( 132.0000000000000000, 69.00000000000000000, 110.0000000000000000 ) ) ;
#4358=ORIENTED_EDGE ( 'NONE', *, *, #61, .T. ) ;
#4386=CIRCLE ( 'NONE', #4165, 24.99999999999999289 ) ;
#4427=CARTESIAN_POINT ( 'NONE',  ( 132.0000000000000000, 69.00000000000000000, 110.0000000000000000 ) ) ;
#4468=ORIENTED_EDGE ( 'NONE', *, *, #4580, .T. ) ;
#4478=AXIS2_PLACEMENT_3D ( 'NONE', #3090, #5058, #5506 ) ;
#4503=DIRECTION ( 'NONE',  ( 1.000000000000000000, 0.000000000000000000, 0.000000000000000000 ) ) ;
#4508=LINE ( 'NONE', #109, #3917 ) ;
#4514=EDGE_LOOP ( 'NONE', ( #1665, #782, #5163, #2375, #5340, #1960, #659, #898, #5943, #3717, #3849, #5113, #2814, #1851 ) ) ;
#4522=LINE ( 'NONE', #935, #3153 ) ;
#4524=ORIENTED_EDGE ( 'NONE', *, *, #2354, .T. ) ;
#4548=AXIS2_PLACEMENT_3D ( 'NONE', #2362, #1464, #3006 ) ;
#4549=EDGE_CURVE ( 'NONE', #3788, #2635, #2140, .T. ) ;
#4552=CYLINDRICAL_SURFACE ( 'NONE', #4804, 24.99999999999999289 ) ;
#4556=VERTEX_POINT ( 'NONE', #172 ) ;
#4561=CARTESIAN_POINT ( 'NONE',  ( 279.0000000000000000, 0.000000000000000000, 0.000000000000000000 ) ) ;
#4577=AXIS2_PLACEMENT_3D ( 'NONE', #3085, #6052, #3594 ) ;
#4579=DIRECTION ( 'NONE',  ( 0.000000000000000000, 0.000000000000000000, 1.000000000000000000 ) ) ;
#4580=EDGE_CURVE ( 'NONE', #6130, #5682, #4822, .T. ) ;
#4582=DIRECTION ( 'NONE',  ( -0.000000000000000000, -0.000000000000000000, -1.000000000000000000 ) ) ;
#4588=MANIFOLD_SOLID_BREP ( 'Fillet1', #838 ) ;
#4596=ADVANCED_FACE ( 'NONE', ( #1417 ), #5359, .F. ) ;
#4611=ORIENTED_EDGE ( 'NONE', *, *, #6219, .F. ) ;
#4638=CARTESIAN_POINT ( 'NONE',  ( 265.0000000000000000, 14.00000000000000000, 0.000000000000000000 ) ) ;
#4651=EDGE_LOOP ( 'NONE', ( #4016, #3476, #1543, #6337 ) ) ;
#4656=EDGE_CURVE ( 'NONE', #4195, #4556, #6226, .T. ) ;
#4666=VERTEX_POINT ( 'NONE', #1841 ) ;
#4668=CARTESIAN_POINT ( 'NONE',  ( 0.000000000000000000, 69.00000000000000000, 0.000000000000000000 ) ) ;
#4669=LINE ( 'NONE', #6195, #654 ) ;
#4673=FACE_OUTER_BOUND ( 'NONE', #6216, .T. ) ;
#4709=ORIENTED_EDGE ( 'NONE', *, *, #4549, .F. ) ;
#4728=FACE_OUTER_BOUND ( 'NONE', #5305, .T. ) ;
#4736=ORIENTED_EDGE ( 'NONE', *, *, #1122, .T. ) ;
#4774=CARTESIAN_POINT ( 'NONE',  ( 17.00000000000000000, 69.00000000000000000, 0.000000000000000000 ) ) ;
#4804=AXIS2_PLACEMENT_3D ( 'NONE', #4060, #3929, #154 ) ;
#4822=CIRCLE ( 'NONE', #5650, 25.00000000000000000 ) ;
#4824=DIRECTION ( 'NONE',  ( -0.000000000000000000, -0.000000000000000000, -1.000000000000000000 ) ) ;
#4835=ADVANCED_FACE ( 'NONE', ( #895 ), #4299, .T. ) ;
#4851=ORIENTED_EDGE ( 'NONE', *, *, #4656, .T. ) ;
#4865=FACE_OUTER_BOUND ( 'NONE', #4651, .T. ) ;
#4870=LINE ( 'NONE', #2360, #1101 ) ;
#4943=PLANE ( 'NONE',  #3981 ) ;
#4948=ORIENTED_EDGE ( 'NONE', *, *, #860, .F. ) ;
#4949=ORIENTED_EDGE ( 'NONE', *, *, #1937, .F. ) ;
#4961=VERTEX_POINT ( 'NONE', #3434 ) ;
#4992=ORIENTED_EDGE ( 'NONE', *, *, #100, .T. ) ;
#5003=VERTEX_POINT ( 'NONE', #1474 ) ;
#5010=PRODUCT_DEFINITION_CONTEXT ( 'detailed design', #167, 'design' ) ;
#5035=VECTOR ( 'NONE', #6204, 1000.000000000000000 ) ;
#5056=CARTESIAN_POINT ( 'NONE',  ( 279.0000000000000000, 14.00000000000000000, 0.000000000000000000 ) ) ;
#5057=VERTEX_POINT ( 'NONE', #85 ) ;
#5058=DIRECTION ( 'NONE',  ( 0.000000000000000000, 0.000000000000000000, 1.000000000000000000 ) ) ;
#5063=DIRECTION ( 'NONE',  ( -0.000000000000000000, -0.000000000000000000, -1.000000000000000000 ) ) ;
#5065=LINE ( 'NONE', #1576, #3714 ) ;
#5079=CARTESIAN_POINT ( 'NONE',  ( 67.00000000000000000, 69.00000000000000000, 110.0000000000000000 ) ) ;
#5080=CARTESIAN_POINT ( 'NONE',  ( 82.00000000000001421, 69.00000000000000000, 110.0000000000000000 ) ) ;
#5090=VERTEX_POINT ( 'NONE', #1198 ) ;
#5109=PLANE ( 'NONE',  #4095 ) ;
#5113=ORIENTED_EDGE ( 'NONE', *, *, #3629, .F. ) ;
#5115=VECTOR ( 'NONE', #1586, 1000.000000000000000 ) ;
#5125=ORIENTED_EDGE ( 'NONE', *, *, #6249, .F. ) ;
#5134=ORIENTED_EDGE ( 'NONE', *, *, #47, .T. ) ;
#5139=VECTOR ( 'NONE', #5594, 1000.000000000000000 ) ;
#5150=PRODUCT_CONTEXT ( 'NONE', #3699, 'mechanical' ) ;
#5156=VECTOR ( 'NONE', #5546, 1000.000000000000000 ) ;
#5158=UNCERTAINTY_MEASURE_WITH_UNIT (LENGTH_MEASURE( 1.000000000000000082E-05 ), #5187, 'distance_accuracy_value', 'NONE');
#5163=ORIENTED_EDGE ( 'NONE', *, *, #1261, .F. ) ;
#5175=CARTESIAN_POINT ( 'NONE',  ( 67.00000000000000000, 69.00000000000000000, 0.000000000000000000 ) ) ;
#5186=ORIENTED_EDGE ( 'NONE', *, *, #118, .F. ) ;
#5187=( LENGTH_UNIT ( ) NAMED_UNIT ( * ) SI_UNIT ( .MILLI., .METRE. ) );
#5207=ORIENTED_EDGE ( 'NONE', *, *, #23, .T. ) ;
#5225=CARTESIAN_POINT ( 'NONE',  ( 42.00000000000000000, 69.00000000000000000, 110.0000000000000000 ) ) ;
#5240=( GEOMETRIC_REPRESENTATION_CONTEXT ( 3 ) GLOBAL_UNCERTAINTY_ASSIGNED_CONTEXT ( ( #1733 ) ) GLOBAL_UNIT_ASSIGNED_CONTEXT ( ( #3154, #3313, #2893 ) ) REPRESENTATION_CONTEXT ( 'NONE', 'WORKASPACE' ) );
#5260=ORIENTED_EDGE ( 'NONE', *, *, #3629, .T. ) ;
#5261=DIRECTION ( 'NONE',  ( -1.000000000000000000, -0.000000000000000000, -0.000000000000000000 ) ) ;
#5271=VERTEX_POINT ( 'NONE', #2775 ) ;
#5272=EDGE_CURVE ( 'NONE', #2635, #4666, #1822, .T. ) ;
#5281=EDGE_LOOP ( 'NONE', ( #742, #2745, #5125, #6207 ) ) ;
#5284=DIRECTION ( 'NONE',  ( -1.000000000000000000, 0.000000000000000000, 0.000000000000000000 ) ) ;
#5285=PLANE ( 'NONE',  #111 ) ;
#5298=ORIENTED_EDGE ( 'NONE', *, *, #3532, .T. ) ;
#5305=EDGE_LOOP ( 'NONE', ( #4736, #4524, #696, #4023 ) ) ;
#5323=CIRCLE ( 'NONE', #6136, 24.99999999999999289 ) ;
#5324=DIRECTION ( 'NONE',  ( 0.000000000000000000, -0.000000000000000000, -1.000000000000000000 ) ) ;
#5340=ORIENTED_EDGE ( 'NONE', *, *, #1122, .F. ) ;
#5350=CARTESIAN_POINT ( 'NONE',  ( 107.0000000000000142, 69.00000000000000000, 0.000000000000000000 ) ) ;
#5359=PLANE ( 'NONE',  #5760 ) ;
#5405=PLANE ( 'NONE',  #1865 ) ;
#5414=ORIENTED_EDGE ( 'NONE', *, *, #40, .T. ) ;
#5417=DIRECTION ( 'NONE',  ( 1.000000000000000000, 0.000000000000000000, 0.000000000000000000 ) ) ;
#5465=ORIENTED_EDGE ( 'NONE', *, *, #1323, .T. ) ;
#5466=VECTOR ( 'NONE', #2431, 1000.000000000000000 ) ;
#5506=DIRECTION ( 'NONE',  ( 1.000000000000000000, 0.000000000000000000, -0.000000000000000000 ) ) ;
#5511=DIRECTION ( 'NONE',  ( 0.000000000000000000, 0.000000000000000000, -1.000000000000000000 ) ) ;
#5518=EDGE_LOOP ( 'NONE', ( #6137, #57, #4948, #194 ) ) ;
#5539=ADVANCED_FACE ( 'NONE', ( #3519 ), #4943, .F. ) ;
#5546=DIRECTION ( 'NONE',  ( -0.000000000000000000, -0.000000000000000000, -1.000000000000000000 ) ) ;
#5560=CARTESIAN_POINT ( 'NONE',  ( 262.0000000000000000, 68.99999999999997158, 110.0000000000000000 ) ) ;
#5575=CARTESIAN_POINT ( 'NONE',  ( 0.000000000000000000, 0.000000000000000000, 0.000000000000000000 ) ) ;
#5587=ADVANCED_FACE ( 'NONE', ( #1468 ), #2937, .F. ) ;
#5594=DIRECTION ( 'NONE',  ( -1.000000000000000000, -0.000000000000000000, -0.000000000000000000 ) ) ;
#5607=LINE ( 'NONE', #1673, #5156 ) ;
#5612=CIRCLE ( 'NONE', #682, 24.99999999999999289 ) ;
#5650=AXIS2_PLACEMENT_3D ( 'NONE', #5674, #4115, #1699 ) ;
#5674=CARTESIAN_POINT ( 'NONE',  ( 42.00000000000000000, 69.00000000000000000, 0.000000000000000000 ) ) ;
#5682=VERTEX_POINT ( 'NONE', #4774 ) ;
#5698=EDGE_CURVE ( 'NONE', #1574, #4961, #4249, .T. ) ;
#5699=CARTESIAN_POINT ( 'NONE',  ( 279.0000000000000000, 68.99999999999997158, 110.0000000000000000 ) ) ;
#5731=EDGE_LOOP ( 'NONE', ( #3141, #2334, #5414, #2099, #2980, #1867, #5207, #4992, #1497, #4851, #1967, #3424, #2808, #2620 ) ) ;
#5749=EDGE_CURVE ( 'NONE', #4236, #5889, #2355, .T. ) ;
#5760=AXIS2_PLACEMENT_3D ( 'NONE', #6288, #1285, #5324 ) ;
#5793=ORIENTED_EDGE ( 'NONE', *, *, #499, .F. ) ;
#5808=DIRECTION ( 'NONE',  ( 0.000000000000000000, 0.000000000000000000, 1.000000000000000000 ) ) ;
#5809=DIRECTION ( 'NONE',  ( -0.000000000000000000, -0.000000000000000000, -1.000000000000000000 ) ) ;
#5826=ADVANCED_FACE ( 'NONE', ( #3416 ), #1485, .F. ) ;
#5843=LINE ( 'NONE', #1422, #4167 ) ;
#5860=FACE_OUTER_BOUND ( 'NONE', #5281, .T. ) ;
#5889=VERTEX_POINT ( 'NONE', #3963 ) ;
#5899=CARTESIAN_POINT ( 'NONE',  ( 17.00000000000000000, 69.00000000000000000, 110.0000000000000000 ) ) ;
#5906=EDGE_CURVE ( 'NONE', #4140, #5271, #5843, .T. ) ;
#5931=DIRECTION ( 'NONE',  ( -1.000000000000000000, -0.000000000000000000, -0.000000000000000000 ) ) ;
#5943=ORIENTED_EDGE ( 'NONE', *, *, #2544, .F. ) ;
#5949=DIRECTION ( 'NONE',  ( 0.000000000000000000, -1.000000000000000000, 0.000000000000000000 ) ) ;
#6002=AXIS2_PLACEMENT_3D ( 'NONE', #5225, #2700, #2287 ) ;
#6003=DIRECTION ( 'NONE',  ( -0.000000000000000000, -0.000000000000000000, -1.000000000000000000 ) ) ;
#6011=CARTESIAN_POINT ( 'NONE',  ( 265.0000000000000000, 14.00000000000000000, 110.0000000000000000 ) ) ;
#6018=EDGE_CURVE ( 'NONE', #1144, #3522, #2732, .T. ) ;
#6052=DIRECTION ( 'NONE',  ( -0.000000000000000000, -0.000000000000000000, -1.000000000000000000 ) ) ;
#6060=STYLED_ITEM('',(#6398),#4588);
#6088=CARTESIAN_POINT ( 'NONE',  ( 0.000000000000000000, 14.00000000000000000, 110.0000000000000000 ) ) ;
#6107=FACE_OUTER_BOUND ( 'NONE', #2163, .T. ) ;
#6116=PRODUCT_DEFINITION_FORMATION_WITH_SPECIFIED_SOURCE ( 'ANY', '', #1681, .NOT_KNOWN. ) ;
#6130=VERTEX_POINT ( 'NONE', #1736 ) ;
#6136=AXIS2_PLACEMENT_3D ( 'NONE', #5350, #4824, #6314 ) ;
#6137=ORIENTED_EDGE ( 'NONE', *, *, #1591, .T. ) ;
#6141=ORIENTED_EDGE ( 'NONE', *, *, #3413, .F. ) ;
#6194=CARTESIAN_POINT ( 'NONE',  ( 42.00000000000000000, 69.00000000000000000, 0.000000000000000000 ) ) ;
#6195=CARTESIAN_POINT ( 'NONE',  ( 0.000000000000000000, 69.00000000000000000, 110.0000000000000000 ) ) ;
#6202=ADVANCED_FACE ( 'NONE', ( #3771 ), #1282, .F. ) ;
#6203=CARTESIAN_POINT ( 'NONE',  ( 237.0000000000000284, 68.99999999999997158, 110.0000000000000000 ) ) ;
#6204=DIRECTION ( 'NONE',  ( -0.000000000000000000, -0.000000000000000000, 1.000000000000000000 ) ) ;
#6207=ORIENTED_EDGE ( 'NONE', *, *, #2097, .T. ) ;
#6210=EDGE_CURVE ( 'NONE', #4556, #6130, #4522, .T. ) ;
#6216=EDGE_LOOP ( 'NONE', ( #5260, #4121, #432, #4358 ) ) ;
#6219=EDGE_CURVE ( 'NONE', #4140, #5682, #3558, .T. ) ;
#6226=LINE ( 'NONE', #1808, #919 ) ;
#6249=EDGE_CURVE ( 'NONE', #3522, #4666, #4034, .T. ) ;
#6279=DIRECTION ( 'NONE',  ( 1.000000000000000000, 0.000000000000000000, 0.000000000000000000 ) ) ;
#6288=CARTESIAN_POINT ( 'NONE',  ( 279.0000000000000000, 68.99999999999997158, 110.0000000000000000 ) ) ;
#6314=DIRECTION ( 'NONE',  ( 1.000000000000000000, 0.000000000000000000, 0.000000000000000000 ) ) ;
#6337=ORIENTED_EDGE ( 'NONE', *, *, #1323, .F. ) ;
#6340=DIRECTION ( 'NONE',  ( -0.000000000000000000, -0.000000000000000000, -1.000000000000000000 ) ) ;
#6349=AXIS2_PLACEMENT_3D ( 'NONE', #290, #2242, #4169 ) ;
#6353=DIRECTION ( 'NONE',  ( -0.000000000000000000, -0.000000000000000000, -1.000000000000000000 ) ) ;
#6356=CARTESIAN_POINT ( 'NONE',  ( 279.0000000000000000, 68.99999999999997158, 110.0000000000000000 ) ) ;
#6392=COLOUR_RGB('Sky Blue',0.24,0.69,0.87);
#6393=FILL_AREA_STYLE_COLOUR('',#6392);
#6394=FILL_AREA_STYLE('',(#6393));
#6395=SURFACE_STYLE_FILL_AREA(#6394);
#6396=SURFACE_SIDE_STYLE('',(#6395));
#6397=SURFACE_STYLE_USAGE(.BOTH.,#6396);
#6398=PRESENTATION_STYLE_ASSIGNMENT((#6397));
ENDSEC;
END-ISO-10303-21;
